ISO-10303-21;
HEADER;
/* Generated by software containing ST-Developer
 * from STEP Tools, Inc. (www.steptools.com) 
 */

FILE_DESCRIPTION(
/* description */ ('STEP AP203'),
/* implementation_level */ '2;1');

FILE_NAME(
/* name */ 'P13_Lower_Feed_Nut.step',
/* time_stamp */ '2026-11-15T15:04:01-08:00',
/* author */ (''),
/* organization */ (''),
/* preprocessor_version */ 'ST-DEVELOPER v20.2',
/* originating_system */ 'Autodesk Translation Framework v15.17.0.0',
/* authorisation */ '');

FILE_SCHEMA (('AUTOMOTIVE_DESIGN { 1 0 10303 214 3 1 1 }'));
ENDSEC;

DATA;
#10=MECHANICAL_DESIGN_GEOMETRIC_PRESENTATION_REPRESENTATION('',(#292),#16598);
#214=SHAPE_REPRESENTATION_RELATIONSHIP('SRR','None',#16708,#238);
#238=ADVANCED_BREP_SHAPE_REPRESENTATION('',(#262),#16584);
#262=MANIFOLD_SOLID_BREP('Body1',#9797);
#292=STYLED_ITEM('',(#16834),#262);
#355=FACE_BOUND('',#1738,.T.);
#356=FACE_BOUND('',#1740,.T.);
#615=PLANE('',#10408);
#616=PLANE('',#10409);
#617=PLANE('',#10410);
#618=PLANE('',#10411);
#619=PLANE('',#10412);
#620=PLANE('',#10413);
#1136=FACE_OUTER_BOUND('',#1736,.T.);
#1137=FACE_OUTER_BOUND('',#1737,.T.);
#1138=FACE_OUTER_BOUND('',#1739,.T.);
#1139=FACE_OUTER_BOUND('',#1741,.T.);
#1140=FACE_OUTER_BOUND('',#1742,.T.);
#1141=FACE_OUTER_BOUND('',#1743,.T.);
#1142=FACE_OUTER_BOUND('',#1744,.T.);
#1736=EDGE_LOOP('',(#7677,#7678,#7679,#7680));
#1737=EDGE_LOOP('',(#7681,#7682,#7683,#7684));
#1738=EDGE_LOOP('',(#7685));
#1739=EDGE_LOOP('',(#7686,#7687,#7688,#7689));
#1740=EDGE_LOOP('',(#7690));
#1741=EDGE_LOOP('',(#7691,#7692,#7693,#7694));
#1742=EDGE_LOOP('',(#7695,#7696,#7697,#7698));
#1743=EDGE_LOOP('',(#7699,#7700,#7701,#7702));
#1744=EDGE_LOOP('',(#7703,#7704,#7705,#7706));
#2580=LINE('',#14891,#3628);
#2581=LINE('',#14896,#3629);
#2582=LINE('',#14898,#3630);
#2583=LINE('',#14900,#3631);
#2584=LINE('',#14901,#3632);
#2585=LINE('',#14905,#3633);
#2586=LINE('',#14907,#3634);
#2587=LINE('',#14909,#3635);
#2588=LINE('',#14910,#3636);
#2589=LINE('',#14912,#3637);
#2590=LINE('',#14913,#3638);
#2591=LINE('',#14915,#3639);
#2592=LINE('',#14917,#3640);
#3628=VECTOR('',#12034,5.75);
#3629=VECTOR('',#12039,1000.);
#3630=VECTOR('',#12040,1000.);
#3631=VECTOR('',#12041,1000.);
#3632=VECTOR('',#12042,1000.);
#3633=VECTOR('',#12045,1000.);
#3634=VECTOR('',#12046,1000.);
#3635=VECTOR('',#12047,1000.);
#3636=VECTOR('',#12048,1000.);
#3637=VECTOR('',#12051,1000.);
#3638=VECTOR('',#12052,1000.);
#3639=VECTOR('',#12055,1000.);
#3640=VECTOR('',#12058,1000.);
#4315=CIRCLE('',#10406,5.75);
#4316=CIRCLE('',#10407,5.75);
#4815=VERTEX_POINT('',#14888);
#4816=VERTEX_POINT('',#14890);
#4817=VERTEX_POINT('',#14894);
#4818=VERTEX_POINT('',#14895);
#4819=VERTEX_POINT('',#14897);
#4820=VERTEX_POINT('',#14899);
#4821=VERTEX_POINT('',#14903);
#4822=VERTEX_POINT('',#14904);
#4823=VERTEX_POINT('',#14906);
#4824=VERTEX_POINT('',#14908);
#5851=EDGE_CURVE('',#4815,#4815,#4315,.T.);
#5852=EDGE_CURVE('',#4815,#4816,#2580,.T.);
#5853=EDGE_CURVE('',#4816,#4816,#4316,.T.);
#5854=EDGE_CURVE('',#4817,#4818,#2581,.T.);
#5855=EDGE_CURVE('',#4818,#4819,#2582,.T.);
#5856=EDGE_CURVE('',#4819,#4820,#2583,.T.);
#5857=EDGE_CURVE('',#4820,#4817,#2584,.T.);
#5858=EDGE_CURVE('',#4821,#4822,#2585,.T.);
#5859=EDGE_CURVE('',#4823,#4821,#2586,.T.);
#5860=EDGE_CURVE('',#4824,#4823,#2587,.T.);
#5861=EDGE_CURVE('',#4822,#4824,#2588,.T.);
#5862=EDGE_CURVE('',#4818,#4822,#2589,.T.);
#5863=EDGE_CURVE('',#4817,#4821,#2590,.T.);
#5864=EDGE_CURVE('',#4819,#4824,#2591,.T.);
#5865=EDGE_CURVE('',#4820,#4823,#2592,.T.);
#7677=ORIENTED_EDGE('',*,*,#5851,.T.);
#7678=ORIENTED_EDGE('',*,*,#5852,.T.);
#7679=ORIENTED_EDGE('',*,*,#5853,.F.);
#7680=ORIENTED_EDGE('',*,*,#5852,.F.);
#7681=ORIENTED_EDGE('',*,*,#5854,.T.);
#7682=ORIENTED_EDGE('',*,*,#5855,.T.);
#7683=ORIENTED_EDGE('',*,*,#5856,.T.);
#7684=ORIENTED_EDGE('',*,*,#5857,.T.);
#7685=ORIENTED_EDGE('',*,*,#5851,.F.);
#7686=ORIENTED_EDGE('',*,*,#5858,.F.);
#7687=ORIENTED_EDGE('',*,*,#5859,.F.);
#7688=ORIENTED_EDGE('',*,*,#5860,.F.);
#7689=ORIENTED_EDGE('',*,*,#5861,.F.);
#7690=ORIENTED_EDGE('',*,*,#5853,.T.);
#7691=ORIENTED_EDGE('',*,*,#5858,.T.);
#7692=ORIENTED_EDGE('',*,*,#5862,.F.);
#7693=ORIENTED_EDGE('',*,*,#5854,.F.);
#7694=ORIENTED_EDGE('',*,*,#5863,.T.);
#7695=ORIENTED_EDGE('',*,*,#5861,.T.);
#7696=ORIENTED_EDGE('',*,*,#5864,.F.);
#7697=ORIENTED_EDGE('',*,*,#5855,.F.);
#7698=ORIENTED_EDGE('',*,*,#5862,.T.);
#7699=ORIENTED_EDGE('',*,*,#5860,.T.);
#7700=ORIENTED_EDGE('',*,*,#5865,.F.);
#7701=ORIENTED_EDGE('',*,*,#5856,.F.);
#7702=ORIENTED_EDGE('',*,*,#5864,.T.);
#7703=ORIENTED_EDGE('',*,*,#5859,.T.);
#7704=ORIENTED_EDGE('',*,*,#5863,.F.);
#7705=ORIENTED_EDGE('',*,*,#5857,.F.);
#7706=ORIENTED_EDGE('',*,*,#5865,.T.);
#9208=CYLINDRICAL_SURFACE('',#10405,5.75);
#9461=ADVANCED_FACE('',(#1136),#9208,.F.);
#9462=ADVANCED_FACE('',(#1137,#355),#615,.T.);
#9463=ADVANCED_FACE('',(#1138,#356),#616,.F.);
#9464=ADVANCED_FACE('',(#1139),#617,.F.);
#9465=ADVANCED_FACE('',(#1140),#618,.F.);
#9466=ADVANCED_FACE('',(#1141),#619,.F.);
#9467=ADVANCED_FACE('',(#1142),#620,.F.);
#9797=CLOSED_SHELL('',(#9461,#9462,#9463,#9464,#9465,#9466,#9467));
#10404=AXIS2_PLACEMENT_3D('',#14886,#12028,#12029);
#10405=AXIS2_PLACEMENT_3D('',#14887,#12030,#12031);
#10406=AXIS2_PLACEMENT_3D('',#14889,#12032,#12033);
#10407=AXIS2_PLACEMENT_3D('',#14892,#12035,#12036);
#10408=AXIS2_PLACEMENT_3D('',#14893,#12037,#12038);
#10409=AXIS2_PLACEMENT_3D('',#14902,#12043,#12044);
#10410=AXIS2_PLACEMENT_3D('',#14911,#12049,#12050);
#10411=AXIS2_PLACEMENT_3D('',#14914,#12053,#12054);
#10412=AXIS2_PLACEMENT_3D('',#14916,#12056,#12057);
#10413=AXIS2_PLACEMENT_3D('',#14918,#12059,#12060);
#12028=DIRECTION('axis',(0.,0.,1.));
#12029=DIRECTION('refdir',(1.,0.,0.));
#12030=DIRECTION('center_axis',(-1.,0.,0.));
#12031=DIRECTION('ref_axis',(0.,0.,1.));
#12032=DIRECTION('center_axis',(1.,0.,0.));
#12033=DIRECTION('ref_axis',(0.,0.,-1.));
#12034=DIRECTION('',(-1.,0.,0.));
#12035=DIRECTION('center_axis',(1.,0.,0.));
#12036=DIRECTION('ref_axis',(0.,0.,-1.));
#12037=DIRECTION('center_axis',(1.,0.,0.));
#12038=DIRECTION('ref_axis',(0.,0.,-1.));
#12039=DIRECTION('',(0.,-1.,0.));
#12040=DIRECTION('',(0.,0.,-1.));
#12041=DIRECTION('',(0.,1.,0.));
#12042=DIRECTION('',(0.,0.,1.));
#12043=DIRECTION('center_axis',(1.,0.,0.));
#12044=DIRECTION('ref_axis',(0.,0.,-1.));
#12045=DIRECTION('',(0.,-1.,0.));
#12046=DIRECTION('',(0.,0.,1.));
#12047=DIRECTION('',(0.,1.,0.));
#12048=DIRECTION('',(0.,0.,-1.));
#12049=DIRECTION('center_axis',(0.,0.,-1.));
#12050=DIRECTION('ref_axis',(-1.,0.,0.));
#12051=DIRECTION('',(-1.,0.,0.));
#12052=DIRECTION('',(-1.,0.,0.));
#12053=DIRECTION('center_axis',(0.,1.,0.));
#12054=DIRECTION('ref_axis',(0.,0.,1.));
#12055=DIRECTION('',(-1.,0.,0.));
#12056=DIRECTION('center_axis',(0.,0.,1.));
#12057=DIRECTION('ref_axis',(1.,0.,0.));
#12058=DIRECTION('',(-1.,0.,0.));
#12059=DIRECTION('center_axis',(0.,-1.,0.));
#12060=DIRECTION('ref_axis',(0.,0.,-1.));
#14886=CARTESIAN_POINT('',(0.,0.,0.));
#14887=CARTESIAN_POINT('Origin',(12.,0.,21.));
#14888=CARTESIAN_POINT('',(12.,-7.04171909509728E-16,15.25));
#14889=CARTESIAN_POINT('Origin',(12.,0.,21.));
#14890=CARTESIAN_POINT('',(-12.,-7.04171909509728E-16,15.25));
#14891=CARTESIAN_POINT('',(12.,-7.04171909509728E-16,15.25));
#14892=CARTESIAN_POINT('Origin',(-12.,0.,21.));
#14893=CARTESIAN_POINT('Origin',(12.,0.,0.));
#14894=CARTESIAN_POINT('',(12.,11.,34.3));
#14895=CARTESIAN_POINT('',(12.,-11.,34.3));
#14896=CARTESIAN_POINT('',(12.,-11.,34.3));
#14897=CARTESIAN_POINT('',(12.,-11.,10.3));
#14898=CARTESIAN_POINT('',(12.,-11.,10.3));
#14899=CARTESIAN_POINT('',(12.,11.,10.3));
#14900=CARTESIAN_POINT('',(12.,-11.,10.3));
#14901=CARTESIAN_POINT('',(12.,11.,10.3));
#14902=CARTESIAN_POINT('Origin',(-12.,0.,0.));
#14903=CARTESIAN_POINT('',(-12.,11.,34.3));
#14904=CARTESIAN_POINT('',(-12.,-11.,34.3));
#14905=CARTESIAN_POINT('',(-12.,-11.,34.3));
#14906=CARTESIAN_POINT('',(-12.,11.,10.3));
#14907=CARTESIAN_POINT('',(-12.,11.,10.3));
#14908=CARTESIAN_POINT('',(-12.,-11.,10.3));
#14909=CARTESIAN_POINT('',(-12.,-11.,10.3));
#14910=CARTESIAN_POINT('',(-12.,-11.,10.3));
#14911=CARTESIAN_POINT('Origin',(12.,-11.,34.3));
#14912=CARTESIAN_POINT('',(12.,-11.,34.3));
#14913=CARTESIAN_POINT('',(12.,11.,34.3));
#14914=CARTESIAN_POINT('Origin',(12.,-11.,10.3));
#14915=CARTESIAN_POINT('',(12.,-11.,10.3));
#14916=CARTESIAN_POINT('Origin',(12.,-11.,10.3));
#14917=CARTESIAN_POINT('',(12.,11.,10.3));
#14918=CARTESIAN_POINT('Origin',(12.,11.,10.3));
#16558=UNCERTAINTY_MEASURE_WITH_UNIT(LENGTH_MEASURE(0.01),#16599,
'DISTANCE_ACCURACY_VALUE',
'Maximum model space distance between geometric entities at asserted c
onnectivities');
#16572=UNCERTAINTY_MEASURE_WITH_UNIT(LENGTH_MEASURE(0.01),#16599,
'DISTANCE_ACCURACY_VALUE',
'Maximum model space distance between geometric entities at asserted c
onnectivities');
#16584=(
GEOMETRIC_REPRESENTATION_CONTEXT(3)
GLOBAL_UNCERTAINTY_ASSIGNED_CONTEXT((#16558))
GLOBAL_UNIT_ASSIGNED_CONTEXT((#16599,#16601,#16602))
REPRESENTATION_CONTEXT('','3D')
);
#16598=(
GEOMETRIC_REPRESENTATION_CONTEXT(3)
GLOBAL_UNCERTAINTY_ASSIGNED_CONTEXT((#16572))
GLOBAL_UNIT_ASSIGNED_CONTEXT((#16599,#16601,#16602))
REPRESENTATION_CONTEXT('','3D')
);
#16599=(
LENGTH_UNIT()
NAMED_UNIT(*)
SI_UNIT(.MILLI.,.METRE.)
);
#16601=(
NAMED_UNIT(*)
PLANE_ANGLE_UNIT()
SI_UNIT($,.RADIAN.)
);
#16602=(
NAMED_UNIT(*)
SI_UNIT($,.STERADIAN.)
SOLID_ANGLE_UNIT()
);
#16614=SHAPE_DEFINITION_REPRESENTATION(#16639,#16708);
#16639=PRODUCT_DEFINITION_SHAPE('',$,#16734);
#16708=SHAPE_REPRESENTATION('',(#10404),#16584);
#16722=PRODUCT_DEFINITION_CONTEXT('part definition',#16799,'design');
#16734=PRODUCT_DEFINITION('P13_Lower_Feed_Nut','P13_Lower_Feed_Nut',#16759,
#16722);
#16759=PRODUCT_DEFINITION_FORMATION('',$,#16812);
#16799=APPLICATION_CONTEXT(
'Core Data for Automotive Mechanical Design Process');
#16800=PRODUCT_CONTEXT('part definition',#16799,'mechanical');
#16812=PRODUCT('P13_Lower_Feed_Nut','P13_Lower_Feed_Nut',$,(#16800));
#16834=PRESENTATION_STYLE_ASSIGNMENT((#16843));
#16843=SURFACE_STYLE_USAGE(.BOTH.,#16852);
#16852=SURFACE_SIDE_STYLE('',(#16861));
#16861=SURFACE_STYLE_FILL_AREA(#16870);
#16870=FILL_AREA_STYLE('Light Blue',(#16879));
#16879=FILL_AREA_STYLE_COLOUR('Light Blue',#16888);
#16888=COLOUR_RGB('Light Blue',0.67843137254902,0.847058823529412,0.901960784313726);
ENDSEC;
END-ISO-10303-21;
